ISO-10303-21;
HEADER;
/* Generated by software containing ST-Developer
 * from STEP Tools, Inc. (www.steptools.com) 
 */

FILE_DESCRIPTION(
/* description */ ('Hand drill press frame (manual)'),
/* implementation_level */ '2;1');

FILE_NAME(
/* name */ 'Cap Screw - M6x25.step',
/* time_stamp */ '2026-10-28T03:25:28-07:00',
/* author */ (''),
/* organization */ (''),
/* preprocessor_version */ 'ST-DEVELOPER v20.2',
/* originating_system */ 'Autodesk Translation Framework v15.17.0.0',
/* authorisation */ '');

FILE_SCHEMA (('AUTOMOTIVE_DESIGN { 1 0 10303 214 3 1 1 }'));
ENDSEC;

DATA;
#10=MECHANICAL_DESIGN_GEOMETRIC_PRESENTATION_REPRESENTATION('',(#668),#33299);
#132=ORIENTED_CLOSED_SHELL('',*,#12688,.F.);
#135=BREP_WITH_VOIDS('Body1',#12687,(#132));
#483=CONICAL_SURFACE('',#14239,0.475,0.785398163397449);
#484=CONICAL_SURFACE('',#14243,0.485,0.785398163397448);
#485=CONICAL_SURFACE('',#14247,0.31,0.463647609000806);
#486=CONICAL_SURFACE('',#14251,0.27,0.785398163397448);
#571=SHAPE_REPRESENTATION_RELATIONSHIP('SRR','None',#33533,#616);
#616=ADVANCED_BREP_SHAPE_REPRESENTATION('',(#135),#33295);
#668=STYLED_ITEM('',(#33821),#135);
#883=FACE_BOUND('',#2847,.T.);
#1315=PLANE('',#14237);
#1316=PLANE('',#14245);
#1317=PLANE('',#14253);
#1318=PLANE('',#14254);
#1319=PLANE('',#14255);
#1320=PLANE('',#14256);
#1321=PLANE('',#14257);
#1322=PLANE('',#14258);
#1323=PLANE('',#14259);
#1324=PLANE('',#14260);
#1325=PLANE('',#14261);
#1990=FACE_OUTER_BOUND('',#2842,.T.);
#1991=FACE_OUTER_BOUND('',#2843,.T.);
#1992=FACE_OUTER_BOUND('',#2844,.T.);
#1993=FACE_OUTER_BOUND('',#2845,.T.);
#1994=FACE_OUTER_BOUND('',#2846,.T.);
#1995=FACE_OUTER_BOUND('',#2848,.T.);
#1996=FACE_OUTER_BOUND('',#2849,.T.);
#1997=FACE_OUTER_BOUND('',#2850,.T.);
#1998=FACE_OUTER_BOUND('',#2851,.T.);
#1999=FACE_OUTER_BOUND('',#2852,.T.);
#2000=FACE_OUTER_BOUND('',#2853,.T.);
#2001=FACE_OUTER_BOUND('',#2854,.T.);
#2002=FACE_OUTER_BOUND('',#2855,.T.);
#2003=FACE_OUTER_BOUND('',#2856,.T.);
#2004=FACE_OUTER_BOUND('',#2857,.T.);
#2005=FACE_OUTER_BOUND('',#2858,.T.);
#2006=FACE_OUTER_BOUND('',#2859,.T.);
#2842=EDGE_LOOP('',(#11645));
#2843=EDGE_LOOP('',(#11646,#11647,#11648,#11649));
#2844=EDGE_LOOP('',(#11650,#11651,#11652,#11653));
#2845=EDGE_LOOP('',(#11654,#11655,#11656,#11657));
#2846=EDGE_LOOP('',(#11658));
#2847=EDGE_LOOP('',(#11659));
#2848=EDGE_LOOP('',(#11660,#11661,#11662,#11663));
#2849=EDGE_LOOP('',(#11664,#11665,#11666,#11667));
#2850=EDGE_LOOP('',(#11668,#11669,#11670,#11671));
#2851=EDGE_LOOP('',(#11672));
#2852=EDGE_LOOP('',(#11673,#11674,#11675,#11676));
#2853=EDGE_LOOP('',(#11677,#11678,#11679,#11680));
#2854=EDGE_LOOP('',(#11681,#11682,#11683,#11684));
#2855=EDGE_LOOP('',(#11685,#11686,#11687,#11688));
#2856=EDGE_LOOP('',(#11689,#11690,#11691,#11692));
#2857=EDGE_LOOP('',(#11693,#11694,#11695,#11696));
#2858=EDGE_LOOP('',(#11697,#11698,#11699,#11700,#11701,#11702));
#2859=EDGE_LOOP('',(#11703,#11704,#11705,#11706,#11707,#11708));
#3999=LINE('',#32978,#5164);
#4000=LINE('',#32982,#5165);
#4001=LINE('',#32986,#5166);
#4002=LINE('',#32993,#5167);
#4003=LINE('',#32997,#5168);
#4004=LINE('',#33001,#5169);
#4005=LINE('',#33006,#5170);
#4006=LINE('',#33008,#5171);
#4007=LINE('',#33010,#5172);
#4008=LINE('',#33011,#5173);
#4009=LINE('',#33014,#5174);
#4010=LINE('',#33016,#5175);
#4011=LINE('',#33017,#5176);
#4012=LINE('',#33020,#5177);
#4013=LINE('',#33022,#5178);
#4014=LINE('',#33023,#5179);
#4015=LINE('',#33026,#5180);
#4016=LINE('',#33028,#5181);
#4017=LINE('',#33029,#5182);
#4018=LINE('',#33032,#5183);
#4019=LINE('',#33034,#5184);
#4020=LINE('',#33035,#5185);
#4021=LINE('',#33037,#5186);
#4022=LINE('',#33038,#5187);
#5164=VECTOR('',#17588,0.475);
#5165=VECTOR('',#17593,0.5);
#5166=VECTOR('',#17598,0.485);
#5167=VECTOR('',#17607,0.31);
#5168=VECTOR('',#17612,0.3);
#5169=VECTOR('',#17617,0.27);
#5170=VECTOR('',#17622,1.);
#5171=VECTOR('',#17623,1.);
#5172=VECTOR('',#17624,1.);
#5173=VECTOR('',#17625,1.);
#5174=VECTOR('',#17628,1.);
#5175=VECTOR('',#17629,1.);
#5176=VECTOR('',#17630,1.);
#5177=VECTOR('',#17633,1.);
#5178=VECTOR('',#17634,1.);
#5179=VECTOR('',#17635,1.);
#5180=VECTOR('',#17638,1.);
#5181=VECTOR('',#17639,1.);
#5182=VECTOR('',#17640,1.);
#5183=VECTOR('',#17643,1.);
#5184=VECTOR('',#17644,1.);
#5185=VECTOR('',#17645,1.);
#5186=VECTOR('',#17648,1.);
#5187=VECTOR('',#17649,1.);
#5593=CIRCLE('',#14238,0.45);
#5594=CIRCLE('',#14240,0.5);
#5595=CIRCLE('',#14242,0.5);
#5596=CIRCLE('',#14244,0.47);
#5597=CIRCLE('',#14246,0.32);
#5598=CIRCLE('',#14248,0.2942);
#5599=CIRCLE('',#14250,0.2942);
#5600=CIRCLE('',#14252,0.24);
#6695=VERTEX_POINT('',#32973);
#6696=VERTEX_POINT('',#32976);
#6697=VERTEX_POINT('',#32980);
#6698=VERTEX_POINT('',#32984);
#6699=VERTEX_POINT('',#32988);
#6700=VERTEX_POINT('',#32991);
#6701=VERTEX_POINT('',#32995);
#6702=VERTEX_POINT('',#32999);
#6703=VERTEX_POINT('',#33004);
#6704=VERTEX_POINT('',#33005);
#6705=VERTEX_POINT('',#33007);
#6706=VERTEX_POINT('',#33009);
#6707=VERTEX_POINT('',#33013);
#6708=VERTEX_POINT('',#33015);
#6709=VERTEX_POINT('',#33019);
#6710=VERTEX_POINT('',#33021);
#6711=VERTEX_POINT('',#33025);
#6712=VERTEX_POINT('',#33027);
#6713=VERTEX_POINT('',#33031);
#6714=VERTEX_POINT('',#33033);
#8351=EDGE_CURVE('',#6695,#6695,#5593,.T.);
#8352=EDGE_CURVE('',#6696,#6696,#5594,.T.);
#8353=EDGE_CURVE('',#6696,#6695,#3999,.T.);
#8354=EDGE_CURVE('',#6697,#6697,#5595,.T.);
#8355=EDGE_CURVE('',#6697,#6696,#4000,.T.);
#8356=EDGE_CURVE('',#6698,#6698,#5596,.T.);
#8357=EDGE_CURVE('',#6698,#6697,#4001,.T.);
#8358=EDGE_CURVE('',#6699,#6699,#5597,.T.);
#8359=EDGE_CURVE('',#6700,#6700,#5598,.F.);
#8360=EDGE_CURVE('',#6700,#6699,#4002,.T.);
#8361=EDGE_CURVE('',#6701,#6701,#5599,.F.);
#8362=EDGE_CURVE('',#6701,#6700,#4003,.T.);
#8363=EDGE_CURVE('',#6702,#6702,#5600,.T.);
#8364=EDGE_CURVE('',#6702,#6701,#4004,.T.);
#8365=EDGE_CURVE('',#6703,#6704,#4005,.T.);
#8366=EDGE_CURVE('',#6704,#6705,#4006,.T.);
#8367=EDGE_CURVE('',#6705,#6706,#4007,.T.);
#8368=EDGE_CURVE('',#6703,#6706,#4008,.T.);
#8369=EDGE_CURVE('',#6704,#6707,#4009,.T.);
#8370=EDGE_CURVE('',#6707,#6708,#4010,.T.);
#8371=EDGE_CURVE('',#6708,#6705,#4011,.T.);
#8372=EDGE_CURVE('',#6707,#6709,#4012,.T.);
#8373=EDGE_CURVE('',#6709,#6710,#4013,.T.);
#8374=EDGE_CURVE('',#6710,#6708,#4014,.T.);
#8375=EDGE_CURVE('',#6709,#6711,#4015,.T.);
#8376=EDGE_CURVE('',#6711,#6712,#4016,.T.);
#8377=EDGE_CURVE('',#6712,#6710,#4017,.T.);
#8378=EDGE_CURVE('',#6711,#6713,#4018,.T.);
#8379=EDGE_CURVE('',#6713,#6714,#4019,.T.);
#8380=EDGE_CURVE('',#6714,#6712,#4020,.T.);
#8381=EDGE_CURVE('',#6713,#6703,#4021,.T.);
#8382=EDGE_CURVE('',#6706,#6714,#4022,.T.);
#11645=ORIENTED_EDGE('',*,*,#8351,.F.);
#11646=ORIENTED_EDGE('',*,*,#8352,.F.);
#11647=ORIENTED_EDGE('',*,*,#8353,.T.);
#11648=ORIENTED_EDGE('',*,*,#8351,.T.);
#11649=ORIENTED_EDGE('',*,*,#8353,.F.);
#11650=ORIENTED_EDGE('',*,*,#8354,.F.);
#11651=ORIENTED_EDGE('',*,*,#8355,.T.);
#11652=ORIENTED_EDGE('',*,*,#8352,.T.);
#11653=ORIENTED_EDGE('',*,*,#8355,.F.);
#11654=ORIENTED_EDGE('',*,*,#8356,.F.);
#11655=ORIENTED_EDGE('',*,*,#8357,.T.);
#11656=ORIENTED_EDGE('',*,*,#8354,.T.);
#11657=ORIENTED_EDGE('',*,*,#8357,.F.);
#11658=ORIENTED_EDGE('',*,*,#8356,.T.);
#11659=ORIENTED_EDGE('',*,*,#8358,.F.);
#11660=ORIENTED_EDGE('',*,*,#8359,.F.);
#11661=ORIENTED_EDGE('',*,*,#8360,.T.);
#11662=ORIENTED_EDGE('',*,*,#8358,.T.);
#11663=ORIENTED_EDGE('',*,*,#8360,.F.);
#11664=ORIENTED_EDGE('',*,*,#8361,.F.);
#11665=ORIENTED_EDGE('',*,*,#8362,.T.);
#11666=ORIENTED_EDGE('',*,*,#8359,.T.);
#11667=ORIENTED_EDGE('',*,*,#8362,.F.);
#11668=ORIENTED_EDGE('',*,*,#8363,.F.);
#11669=ORIENTED_EDGE('',*,*,#8364,.T.);
#11670=ORIENTED_EDGE('',*,*,#8361,.T.);
#11671=ORIENTED_EDGE('',*,*,#8364,.F.);
#11672=ORIENTED_EDGE('',*,*,#8363,.T.);
#11673=ORIENTED_EDGE('',*,*,#8365,.T.);
#11674=ORIENTED_EDGE('',*,*,#8366,.T.);
#11675=ORIENTED_EDGE('',*,*,#8367,.T.);
#11676=ORIENTED_EDGE('',*,*,#8368,.F.);
#11677=ORIENTED_EDGE('',*,*,#8369,.T.);
#11678=ORIENTED_EDGE('',*,*,#8370,.T.);
#11679=ORIENTED_EDGE('',*,*,#8371,.T.);
#11680=ORIENTED_EDGE('',*,*,#8366,.F.);
#11681=ORIENTED_EDGE('',*,*,#8372,.T.);
#11682=ORIENTED_EDGE('',*,*,#8373,.T.);
#11683=ORIENTED_EDGE('',*,*,#8374,.T.);
#11684=ORIENTED_EDGE('',*,*,#8370,.F.);
#11685=ORIENTED_EDGE('',*,*,#8375,.T.);
#11686=ORIENTED_EDGE('',*,*,#8376,.T.);
#11687=ORIENTED_EDGE('',*,*,#8377,.T.);
#11688=ORIENTED_EDGE('',*,*,#8373,.F.);
#11689=ORIENTED_EDGE('',*,*,#8378,.T.);
#11690=ORIENTED_EDGE('',*,*,#8379,.T.);
#11691=ORIENTED_EDGE('',*,*,#8380,.T.);
#11692=ORIENTED_EDGE('',*,*,#8376,.F.);
#11693=ORIENTED_EDGE('',*,*,#8381,.T.);
#11694=ORIENTED_EDGE('',*,*,#8368,.T.);
#11695=ORIENTED_EDGE('',*,*,#8382,.T.);
#11696=ORIENTED_EDGE('',*,*,#8379,.F.);
#11697=ORIENTED_EDGE('',*,*,#8381,.F.);
#11698=ORIENTED_EDGE('',*,*,#8378,.F.);
#11699=ORIENTED_EDGE('',*,*,#8375,.F.);
#11700=ORIENTED_EDGE('',*,*,#8372,.F.);
#11701=ORIENTED_EDGE('',*,*,#8369,.F.);
#11702=ORIENTED_EDGE('',*,*,#8365,.F.);
#11703=ORIENTED_EDGE('',*,*,#8382,.F.);
#11704=ORIENTED_EDGE('',*,*,#8367,.F.);
#11705=ORIENTED_EDGE('',*,*,#8371,.F.);
#11706=ORIENTED_EDGE('',*,*,#8374,.F.);
#11707=ORIENTED_EDGE('',*,*,#8377,.F.);
#11708=ORIENTED_EDGE('',*,*,#8380,.F.);
#11942=CYLINDRICAL_SURFACE('',#14241,0.5);
#11943=CYLINDRICAL_SURFACE('',#14249,0.2942);
#12599=ADVANCED_FACE('',(#1990),#1315,.T.);
#12600=ADVANCED_FACE('',(#1991),#483,.T.);
#12601=ADVANCED_FACE('',(#1992),#11942,.T.);
#12602=ADVANCED_FACE('',(#1993),#484,.T.);
#12603=ADVANCED_FACE('',(#1994,#883),#1316,.T.);
#12604=ADVANCED_FACE('',(#1995),#485,.T.);
#12605=ADVANCED_FACE('',(#1996),#11943,.T.);
#12606=ADVANCED_FACE('',(#1997),#486,.T.);
#12607=ADVANCED_FACE('',(#1998),#1317,.T.);
#12608=ADVANCED_FACE('',(#1999),#1318,.F.);
#12609=ADVANCED_FACE('',(#2000),#1319,.F.);
#12610=ADVANCED_FACE('',(#2001),#1320,.F.);
#12611=ADVANCED_FACE('',(#2002),#1321,.F.);
#12612=ADVANCED_FACE('',(#2003),#1322,.F.);
#12613=ADVANCED_FACE('',(#2004),#1323,.F.);
#12614=ADVANCED_FACE('',(#2005),#1324,.F.);
#12615=ADVANCED_FACE('',(#2006),#1325,.F.);
#12687=CLOSED_SHELL('',(#12599,#12600,#12601,#12602,#12603,#12604,#12605,
#12606,#12607));
#12688=CLOSED_SHELL('',(#12608,#12609,#12610,#12611,#12612,#12613,#12614,
#12615));
#14236=AXIS2_PLACEMENT_3D('',#32971,#17578,#17579);
#14237=AXIS2_PLACEMENT_3D('',#32972,#17580,#17581);
#14238=AXIS2_PLACEMENT_3D('',#32974,#17582,#17583);
#14239=AXIS2_PLACEMENT_3D('',#32975,#17584,#17585);
#14240=AXIS2_PLACEMENT_3D('',#32977,#17586,#17587);
#14241=AXIS2_PLACEMENT_3D('',#32979,#17589,#17590);
#14242=AXIS2_PLACEMENT_3D('',#32981,#17591,#17592);
#14243=AXIS2_PLACEMENT_3D('',#32983,#17594,#17595);
#14244=AXIS2_PLACEMENT_3D('',#32985,#17596,#17597);
#14245=AXIS2_PLACEMENT_3D('',#32987,#17599,#17600);
#14246=AXIS2_PLACEMENT_3D('',#32989,#17601,#17602);
#14247=AXIS2_PLACEMENT_3D('',#32990,#17603,#17604);
#14248=AXIS2_PLACEMENT_3D('',#32992,#17605,#17606);
#14249=AXIS2_PLACEMENT_3D('',#32994,#17608,#17609);
#14250=AXIS2_PLACEMENT_3D('',#32996,#17610,#17611);
#14251=AXIS2_PLACEMENT_3D('',#32998,#17613,#17614);
#14252=AXIS2_PLACEMENT_3D('',#33000,#17615,#17616);
#14253=AXIS2_PLACEMENT_3D('',#33002,#17618,#17619);
#14254=AXIS2_PLACEMENT_3D('',#33003,#17620,#17621);
#14255=AXIS2_PLACEMENT_3D('',#33012,#17626,#17627);
#14256=AXIS2_PLACEMENT_3D('',#33018,#17631,#17632);
#14257=AXIS2_PLACEMENT_3D('',#33024,#17636,#17637);
#14258=AXIS2_PLACEMENT_3D('',#33030,#17641,#17642);
#14259=AXIS2_PLACEMENT_3D('',#33036,#17646,#17647);
#14260=AXIS2_PLACEMENT_3D('',#33039,#17650,#17651);
#14261=AXIS2_PLACEMENT_3D('',#33040,#17652,#17653);
#17578=DIRECTION('axis',(0.,0.,1.));
#17579=DIRECTION('refdir',(1.,0.,0.));
#17580=DIRECTION('center_axis',(0.,1.,0.));
#17581=DIRECTION('ref_axis',(0.,0.,1.));
#17582=DIRECTION('center_axis',(0.,-1.,0.));
#17583=DIRECTION('ref_axis',(1.,0.,0.));
#17584=DIRECTION('center_axis',(0.,-1.,0.));
#17585=DIRECTION('ref_axis',(1.,0.,0.));
#17586=DIRECTION('center_axis',(0.,-1.,0.));
#17587=DIRECTION('ref_axis',(1.,0.,0.));
#17588=DIRECTION('',(0.707106781186548,0.707106781186547,8.65956056235494E-17));
#17589=DIRECTION('center_axis',(0.,-1.,0.));
#17590=DIRECTION('ref_axis',(1.,0.,0.));
#17591=DIRECTION('center_axis',(0.,-1.,0.));
#17592=DIRECTION('ref_axis',(1.,0.,0.));
#17593=DIRECTION('',(0.,1.,0.));
#17594=DIRECTION('center_axis',(0.,1.,0.));
#17595=DIRECTION('ref_axis',(1.,0.,0.));
#17596=DIRECTION('center_axis',(0.,-1.,0.));
#17597=DIRECTION('ref_axis',(1.,0.,0.));
#17598=DIRECTION('',(-0.707106781186547,0.707106781186548,-8.65956056235493E-17));
#17599=DIRECTION('center_axis',(0.,-1.,0.));
#17600=DIRECTION('ref_axis',(0.,0.,-1.));
#17601=DIRECTION('center_axis',(0.,-1.,0.));
#17602=DIRECTION('ref_axis',(1.,0.,0.));
#17603=DIRECTION('center_axis',(0.,1.,0.));
#17604=DIRECTION('ref_axis',(1.,0.,0.));
#17605=DIRECTION('center_axis',(0.,1.,0.));
#17606=DIRECTION('ref_axis',(1.,0.,0.));
#17607=DIRECTION('',(-0.447213595499958,0.894427190999916,-5.47678698264203E-17));
#17608=DIRECTION('center_axis',(0.,-1.,0.));
#17609=DIRECTION('ref_axis',(1.,0.,0.));
#17610=DIRECTION('center_axis',(0.,1.,0.));
#17611=DIRECTION('ref_axis',(1.,0.,0.));
#17612=DIRECTION('',(0.,1.,0.));
#17613=DIRECTION('center_axis',(0.,1.,0.));
#17614=DIRECTION('ref_axis',(1.,0.,0.));
#17615=DIRECTION('center_axis',(0.,-1.,0.));
#17616=DIRECTION('ref_axis',(1.,0.,0.));
#17617=DIRECTION('',(-0.707106781186547,0.707106781186548,-8.65956056235493E-17));
#17618=DIRECTION('center_axis',(0.,-1.,0.));
#17619=DIRECTION('ref_axis',(0.,0.,-1.));
#17620=DIRECTION('center_axis',(0.866025403784439,0.,-0.5));
#17621=DIRECTION('ref_axis',(0.5,0.,0.866025403784439));
#17622=DIRECTION('',(-0.5,0.,-0.866025403784439));
#17623=DIRECTION('',(0.,-1.,0.));
#17624=DIRECTION('',(0.5,0.,0.866025403784439));
#17625=DIRECTION('',(0.,-1.,0.));
#17626=DIRECTION('center_axis',(1.92296268638356E-16,0.,-1.));
#17627=DIRECTION('ref_axis',(1.,0.,1.92296268638356E-16));
#17628=DIRECTION('',(-1.,0.,-1.92296268638356E-16));
#17629=DIRECTION('',(0.,-1.,0.));
#17630=DIRECTION('',(1.,0.,1.92296268638356E-16));
#17631=DIRECTION('center_axis',(-0.866025403784439,0.,-0.5));
#17632=DIRECTION('ref_axis',(0.5,0.,-0.866025403784439));
#17633=DIRECTION('',(-0.5,0.,0.866025403784438));
#17634=DIRECTION('',(0.,-1.,0.));
#17635=DIRECTION('',(0.5,0.,-0.866025403784438));
#17636=DIRECTION('center_axis',(-0.866025403784439,0.,0.5));
#17637=DIRECTION('ref_axis',(-0.5,0.,-0.866025403784439));
#17638=DIRECTION('',(0.5,0.,0.866025403784439));
#17639=DIRECTION('',(0.,-1.,0.));
#17640=DIRECTION('',(-0.5,0.,-0.866025403784439));
#17641=DIRECTION('center_axis',(-1.92296268638356E-16,0.,1.));
#17642=DIRECTION('ref_axis',(-1.,0.,-1.92296268638356E-16));
#17643=DIRECTION('',(1.,0.,1.92296268638356E-16));
#17644=DIRECTION('',(0.,-1.,0.));
#17645=DIRECTION('',(-1.,0.,-1.92296268638356E-16));
#17646=DIRECTION('center_axis',(0.866025403784439,0.,0.5));
#17647=DIRECTION('ref_axis',(-0.5,0.,0.866025403784439));
#17648=DIRECTION('',(0.5,0.,-0.866025403784439));
#17649=DIRECTION('',(-0.5,0.,0.866025403784439));
#17650=DIRECTION('center_axis',(0.,1.,0.));
#17651=DIRECTION('ref_axis',(1.,0.,0.));
#17652=DIRECTION('center_axis',(0.,-1.,0.));
#17653=DIRECTION('ref_axis',(0.,0.,-1.));
#32971=CARTESIAN_POINT('',(0.,0.,0.));
#32972=CARTESIAN_POINT('Origin',(0.45,0.6,0.));
#32973=CARTESIAN_POINT('',(-0.45,0.6,-5.51091059616309E-17));
#32974=CARTESIAN_POINT('Origin',(0.,0.6,0.));
#32975=CARTESIAN_POINT('Origin',(0.,0.575,0.));
#32976=CARTESIAN_POINT('',(-0.5,0.55,-6.12323399573677E-17));
#32977=CARTESIAN_POINT('Origin',(0.,0.55,0.));
#32978=CARTESIAN_POINT('',(-0.475,0.575,-5.81707229594993E-17));
#32979=CARTESIAN_POINT('Origin',(0.,0.29,0.));
#32980=CARTESIAN_POINT('',(-0.5,0.0299999999999998,-6.12323399573677E-17));
#32981=CARTESIAN_POINT('Origin',(0.,0.0299999999999998,0.));
#32982=CARTESIAN_POINT('',(-0.5,0.29,-6.12323399573677E-17));
#32983=CARTESIAN_POINT('Origin',(0.,0.0150000000000001,0.));
#32984=CARTESIAN_POINT('',(-0.47,7.11236625150491E-17,-5.75583995599256E-17));
#32985=CARTESIAN_POINT('Origin',(0.,0.,0.));
#32986=CARTESIAN_POINT('',(-0.485,0.0150000000000001,-5.93953697586466E-17));
#32987=CARTESIAN_POINT('Origin',(0.32,0.,0.));
#32988=CARTESIAN_POINT('',(-0.32,-6.93889390390723E-18,-3.91886975727153E-17));
#32989=CARTESIAN_POINT('Origin',(0.,0.,0.));
#32990=CARTESIAN_POINT('Origin',(0.,-0.02,0.));
#32991=CARTESIAN_POINT('',(-0.2942,-0.0515999999999999,3.60291088309151E-17));
#32992=CARTESIAN_POINT('Origin',(0.,-0.0515999999999999,0.));
#32993=CARTESIAN_POINT('',(-0.31,-0.02,-3.7964050773568E-17));
#32994=CARTESIAN_POINT('Origin',(0.,-1.24,0.));
#32995=CARTESIAN_POINT('',(-0.2942,-2.4458,3.60291088309151E-17));
#32996=CARTESIAN_POINT('Origin',(0.,-2.4458,0.));
#32997=CARTESIAN_POINT('',(-0.2942,-1.24,-3.60291088309151E-17));
#32998=CARTESIAN_POINT('Origin',(0.,-2.47,0.));
#32999=CARTESIAN_POINT('',(-0.24,-2.5,-2.93915231795365E-17));
#33000=CARTESIAN_POINT('Origin',(0.,-2.5,0.));
#33001=CARTESIAN_POINT('',(-0.27,-2.47,-3.30654635769785E-17));
#33002=CARTESIAN_POINT('Origin',(0.,-2.5,0.));
#33003=CARTESIAN_POINT('Origin',(0.144337567297406,-0.6,-0.25));
#33004=CARTESIAN_POINT('',(0.288675134594813,-0.6,0.));
#33005=CARTESIAN_POINT('',(0.144337567297406,-0.6,-0.25));
#33006=CARTESIAN_POINT('',(0.288675134594813,-0.6,0.));
#33007=CARTESIAN_POINT('',(0.144337567297406,-0.96,-0.25));
#33008=CARTESIAN_POINT('',(0.144337567297406,-0.6,-0.25));
#33009=CARTESIAN_POINT('',(0.288675134594813,-0.96,0.));
#33010=CARTESIAN_POINT('',(0.288675134594813,-0.96,0.));
#33011=CARTESIAN_POINT('',(0.288675134594813,-0.6,0.));
#33012=CARTESIAN_POINT('Origin',(-0.144337567297406,-0.6,-0.25));
#33013=CARTESIAN_POINT('',(-0.144337567297406,-0.6,-0.25));
#33014=CARTESIAN_POINT('',(0.144337567297406,-0.6,-0.25));
#33015=CARTESIAN_POINT('',(-0.144337567297406,-0.96,-0.25));
#33016=CARTESIAN_POINT('',(-0.144337567297406,-0.6,-0.25));
#33017=CARTESIAN_POINT('',(0.144337567297406,-0.96,-0.25));
#33018=CARTESIAN_POINT('Origin',(-0.288675134594813,-0.6,-8.32667268468867E-17));
#33019=CARTESIAN_POINT('',(-0.288675134594813,-0.6,-3.53525079574969E-17));
#33020=CARTESIAN_POINT('',(-0.144337567297406,-0.6,-0.25));
#33021=CARTESIAN_POINT('',(-0.288675134594813,-0.96,-5.55111512312578E-17));
#33022=CARTESIAN_POINT('',(-0.288675134594813,-0.6,-3.53525079574969E-17));
#33023=CARTESIAN_POINT('',(-0.144337567297406,-0.96,-0.25));
#33024=CARTESIAN_POINT('Origin',(-0.144337567297407,-0.6,0.25));
#33025=CARTESIAN_POINT('',(-0.144337567297407,-0.6,0.25));
#33026=CARTESIAN_POINT('',(-0.288675134594813,-0.6,-3.53525079574969E-17));
#33027=CARTESIAN_POINT('',(-0.144337567297407,-0.96,0.25));
#33028=CARTESIAN_POINT('',(-0.144337567297407,-0.6,0.25));
#33029=CARTESIAN_POINT('',(-0.288675134594813,-0.96,-3.53525079574969E-17));
#33030=CARTESIAN_POINT('Origin',(0.144337567297406,-0.6,0.25));
#33031=CARTESIAN_POINT('',(0.144337567297406,-0.6,0.25));
#33032=CARTESIAN_POINT('',(-0.144337567297407,-0.6,0.25));
#33033=CARTESIAN_POINT('',(0.144337567297406,-0.96,0.25));
#33034=CARTESIAN_POINT('',(0.144337567297406,-0.6,0.25));
#33035=CARTESIAN_POINT('',(-0.144337567297407,-0.96,0.25));
#33036=CARTESIAN_POINT('Origin',(0.288675134594813,-0.6,0.));
#33037=CARTESIAN_POINT('',(0.144337567297406,-0.6,0.25));
#33038=CARTESIAN_POINT('',(0.144337567297406,-0.96,0.25));
#33039=CARTESIAN_POINT('Origin',(0.,-0.6,0.));
#33040=CARTESIAN_POINT('Origin',(0.,-0.96,0.));
#33243=UNCERTAINTY_MEASURE_WITH_UNIT(LENGTH_MEASURE(0.001),#33300,
'DISTANCE_ACCURACY_VALUE',
'Maximum model space distance between geometric entities at asserted c
onnectivities');
#33247=UNCERTAINTY_MEASURE_WITH_UNIT(LENGTH_MEASURE(0.001),#33300,
'DISTANCE_ACCURACY_VALUE',
'Maximum model space distance between geometric entities at asserted c
onnectivities');
#33295=(
GEOMETRIC_REPRESENTATION_CONTEXT(3)
GLOBAL_UNCERTAINTY_ASSIGNED_CONTEXT((#33243))
GLOBAL_UNIT_ASSIGNED_CONTEXT((#33300,#33302,#33303))
REPRESENTATION_CONTEXT('','3D')
);
#33299=(
GEOMETRIC_REPRESENTATION_CONTEXT(3)
GLOBAL_UNCERTAINTY_ASSIGNED_CONTEXT((#33247))
GLOBAL_UNIT_ASSIGNED_CONTEXT((#33300,#33302,#33303))
REPRESENTATION_CONTEXT('','3D')
);
#33300=(
LENGTH_UNIT()
NAMED_UNIT(*)
SI_UNIT(.CENTI.,.METRE.)
);
#33302=(
NAMED_UNIT(*)
PLANE_ANGLE_UNIT()
SI_UNIT($,.RADIAN.)
);
#33303=(
NAMED_UNIT(*)
SI_UNIT($,.STERADIAN.)
SOLID_ANGLE_UNIT()
);
#33351=SHAPE_DEFINITION_REPRESENTATION(#33413,#33533);
#33413=PRODUCT_DEFINITION_SHAPE('',$,#33585);
#33533=SHAPE_REPRESENTATION('',(#14236),#33295);
#33537=PRODUCT_DEFINITION_CONTEXT('part definition',#33692,'design');
#33585=PRODUCT_DEFINITION('Cap Screw - M6x25','Cap Screw - M6x25',#33636,
#33537);
#33636=PRODUCT_DEFINITION_FORMATION('',$,#33741);
#33692=APPLICATION_CONTEXT(
'Core Data for Automotive Mechanical Design Process');
#33693=PRODUCT_CONTEXT('part definition',#33692,'mechanical');
#33741=PRODUCT('Cap Screw - M6x25','Cap Screw - M6x25',
'Cap Screw - M6x25',(#33693));
#33815=COLOUR_RGB('Black',0.12,0.14,0.17);
#33816=FILL_AREA_STYLE_COLOUR('',#33815);
#33817=FILL_AREA_STYLE('',(#33816));
#33818=SURFACE_STYLE_FILL_AREA(#33817);
#33819=SURFACE_SIDE_STYLE('',(#33818));
#33820=SURFACE_STYLE_USAGE(.BOTH.,#33819);
#33821=PRESENTATION_STYLE_ASSIGNMENT((#33820));
ENDSEC;
END-ISO-10303-21;
